ISO-10303-21;
HEADER;
FILE_DESCRIPTION((''),'2;1');
FILE_NAME('Cover_Screw_3.step','2026-10-09T10:11:57-07:00',(''),(''),'','','');
FILE_SCHEMA (('AUTOMOTIVE_DESIGN { 1 0 10303 214 3 1 1 }'));
ENDSEC;
DATA;
#10=MECHANICAL_DESIGN_GEOMETRIC_PRESENTATION_REPRESENTATION('',(#131),#13510);
#101=SHAPE_REPRESENTATION_RELATIONSHIP('SRR','None',#13571,#116) ;
#116=ADVANCED_BREP_SHAPE_REPRESENTATION('',(#163),#13503) ;
#131=STYLED_ITEM('',(#13650),#163) ;
#163=MANIFOLD_SOLID_BREP('Body1',#7380) ;
#245=FACE_BOUND('',#1492,.T.) ;
#435=PLANE('',#8233) ;
#436=PLANE('',#8234) ;
#437=PLANE('',#8235) ;
#438=PLANE('',#8236) ;
#439=PLANE('',#8237) ;
#440=PLANE('',#8238) ;
#441=PLANE('',#8239) ;
#442=PLANE('',#8240) ;
#443=PLANE('',#8241) ;
#444=PLANE('',#8242) ;
#445=PLANE('',#8243) ;
#446=PLANE('',#8244) ;
#447=PLANE('',#8245) ;
#448=PLANE('',#8246) ;
#449=PLANE('',#8247) ;
#450=PLANE('',#8248) ;
#451=PLANE('',#8249) ;
#452=PLANE('',#8250) ;
#453=PLANE('',#8251) ;
#642=CYLINDRICAL_SURFACE('',#8224,2.6) ;
#643=CYLINDRICAL_SURFACE('',#8229,1.5) ;
#972=FACE_OUTER_BOUND('',#1478,.T.) ;
#973=FACE_OUTER_BOUND('',#1479,.T.) ;
#974=FACE_OUTER_BOUND('',#1480,.T.) ;
#975=FACE_OUTER_BOUND('',#1481,.T.) ;
#976=FACE_OUTER_BOUND('',#1482,.T.) ;
#977=FACE_OUTER_BOUND('',#1483,.T.) ;
#978=FACE_OUTER_BOUND('',#1484,.T.) ;
#979=FACE_OUTER_BOUND('',#1485,.T.) ;
#980=FACE_OUTER_BOUND('',#1486,.T.) ;
#981=FACE_OUTER_BOUND('',#1487,.T.) ;
#982=FACE_OUTER_BOUND('',#1488,.T.) ;
#983=FACE_OUTER_BOUND('',#1489,.T.) ;
#984=FACE_OUTER_BOUND('',#1490,.T.) ;
#985=FACE_OUTER_BOUND('',#1491,.T.) ;
#986=FACE_OUTER_BOUND('',#1493,.T.) ;
#987=FACE_OUTER_BOUND('',#1494,.T.) ;
#988=FACE_OUTER_BOUND('',#1495,.T.) ;
#989=FACE_OUTER_BOUND('',#1496,.T.) ;
#990=FACE_OUTER_BOUND('',#1497,.T.) ;
#991=FACE_OUTER_BOUND('',#1498,.T.) ;
#992=FACE_OUTER_BOUND('',#1499,.T.) ;
#993=FACE_OUTER_BOUND('',#1500,.T.) ;
#994=FACE_OUTER_BOUND('',#1501,.T.) ;
#1478=EDGE_LOOP('',(#6342,#6343,#6344,#6345)) ;
#1479=EDGE_LOOP('',(#6346,#6347,#6348,#6349)) ;
#1480=EDGE_LOOP('',(#6350,#6351,#6352,#6353)) ;
#1481=EDGE_LOOP('',(#6354,#6355,#6356,#6357)) ;
#1482=EDGE_LOOP('',(#6358)) ;
#1483=EDGE_LOOP('',(#6359,#6360,#6361,#6362)) ;
#1484=EDGE_LOOP('',(#6363,#6364,#6365,#6366)) ;
#1485=EDGE_LOOP('',(#6367,#6368,#6369,#6370)) ;
#1486=EDGE_LOOP('',(#6371,#6372,#6373,#6374)) ;
#1487=EDGE_LOOP('',(#6375,#6376,#6377,#6378)) ;
#1488=EDGE_LOOP('',(#6379,#6380,#6381,#6382)) ;
#1489=EDGE_LOOP('',(#6383,#6384,#6385,#6386)) ;
#1490=EDGE_LOOP('',(#6387,#6388,#6389,#6390)) ;
#1491=EDGE_LOOP('',(#6391)) ;
#1492=EDGE_LOOP('',(#6392,#6393,#6394,#6395,#6396,#6397,#6398,#6399,#6400,
#6401,#6402,#6403)) ;
#1493=EDGE_LOOP('',(#6404,#6405,#6406,#6407)) ;
#1494=EDGE_LOOP('',(#6408,#6409,#6410,#6411)) ;
#1495=EDGE_LOOP('',(#6412,#6413,#6414,#6415)) ;
#1496=EDGE_LOOP('',(#6416,#6417,#6418,#6419)) ;
#1497=EDGE_LOOP('',(#6420,#6421,#6422,#6423)) ;
#1498=EDGE_LOOP('',(#6424,#6425,#6426,#6427)) ;
#1499=EDGE_LOOP('',(#6428,#6429,#6430,#6431)) ;
#1500=EDGE_LOOP('',(#6432,#6433,#6434,#6435)) ;
#1501=EDGE_LOOP('',(#6436,#6437,#6438,#6439)) ;
#2051=LINE('',#12871,#2545) ;
#2052=LINE('',#12875,#2546) ;
#2053=LINE('',#12879,#2547) ;
#2054=LINE('',#12883,#2548) ;
#2055=LINE('',#12889,#2549) ;
#2056=LINE('',#12891,#2550) ;
#2057=LINE('',#12893,#2551) ;
#2058=LINE('',#12894,#2552) ;
#2059=LINE('',#12898,#2553) ;
#2060=LINE('',#12900,#2554) ;
#2061=LINE('',#12902,#2555) ;
#2062=LINE('',#12903,#2556) ;
#2063=LINE('',#12906,#2557) ;
#2064=LINE('',#12908,#2558) ;
#2065=LINE('',#12909,#2559) ;
#2066=LINE('',#12913,#2560) ;
#2067=LINE('',#12914,#2561) ;
#2068=LINE('',#12915,#2562) ;
#2069=LINE('',#12918,#2563) ;
#2070=LINE('',#12919,#2564) ;
#2071=LINE('',#12922,#2565) ;
#2072=LINE('',#12923,#2566) ;
#2073=LINE('',#12926,#2567) ;
#2074=LINE('',#12927,#2568) ;
#2075=LINE('',#12930,#2569) ;
#2076=LINE('',#12931,#2570) ;
#2077=LINE('',#12934,#2571) ;
#2078=LINE('',#12936,#2572) ;
#2079=LINE('',#12937,#2573) ;
#2080=LINE('',#12939,#2574) ;
#2081=LINE('',#12941,#2575) ;
#2082=LINE('',#12942,#2576) ;
#2083=LINE('',#12946,#2577) ;
#2084=LINE('',#12947,#2578) ;
#2085=LINE('',#12948,#2579) ;
#2086=LINE('',#12949,#2580) ;
#2087=LINE('',#12951,#2581) ;
#2088=LINE('',#12952,#2582) ;
#2089=LINE('',#12956,#2583) ;
#2090=LINE('',#12958,#2584) ;
#2091=LINE('',#12960,#2585) ;
#2092=LINE('',#12961,#2586) ;
#2093=LINE('',#12963,#2587) ;
#2094=LINE('',#12965,#2588) ;
#2545=VECTOR('',#10281,2.6) ;
#2546=VECTOR('',#10286,1.5) ;
#2547=VECTOR('',#10291,1.5) ;
#2548=VECTOR('',#10296,1.2) ;
#2549=VECTOR('',#10303,0.99999999999962) ;
#2550=VECTOR('',#10304,1.00000000000035) ;
#2551=VECTOR('',#10305,0.99999999999962) ;
#2552=VECTOR('',#10306,1.00000000000035) ;
#2553=VECTOR('',#10309,0.99999999999962) ;
#2554=VECTOR('',#10310,1.00000000000035) ;
#2555=VECTOR('',#10311,0.99999999999962) ;
#2556=VECTOR('',#10312,1.00000000000035) ;
#2557=VECTOR('',#10315,1.) ;
#2558=VECTOR('',#10316,0.99999999999962) ;
#2559=VECTOR('',#10317,1.) ;
#2560=VECTOR('',#10320,0.99999999999962) ;
#2561=VECTOR('',#10321,1.) ;
#2562=VECTOR('',#10322,1.) ;
#2563=VECTOR('',#10325,0.99999999999962) ;
#2564=VECTOR('',#10326,1.) ;
#2565=VECTOR('',#10329,0.99999999999962) ;
#2566=VECTOR('',#10330,1.) ;
#2567=VECTOR('',#10333,1.) ;
#2568=VECTOR('',#10334,0.99999999999962) ;
#2569=VECTOR('',#10337,1.) ;
#2570=VECTOR('',#10338,0.99999999999962) ;
#2571=VECTOR('',#10341,0.99999999999962) ;
#2572=VECTOR('',#10342,0.99999999999962) ;
#2573=VECTOR('',#10343,0.99999999999962) ;
#2574=VECTOR('',#10344,0.99999999999962) ;
#2575=VECTOR('',#10345,0.99999999999962) ;
#2576=VECTOR('',#10346,0.99999999999962) ;
#2577=VECTOR('',#10349,0.99999999999962) ;
#2578=VECTOR('',#10350,1.00000000000035) ;
#2579=VECTOR('',#10351,0.99999999999962) ;
#2580=VECTOR('',#10352,1.00000000000035) ;
#2581=VECTOR('',#10355,1.) ;
#2582=VECTOR('',#10356,1.) ;
#2583=VECTOR('',#10363,0.99999999999962) ;
#2584=VECTOR('',#10364,1.00000000000035) ;
#2585=VECTOR('',#10365,0.99999999999962) ;
#2586=VECTOR('',#10366,1.00000000000035) ;
#2587=VECTOR('',#10369,1.) ;
#2588=VECTOR('',#10372,1.) ;
#2971=CIRCLE('',#8225,2.6) ;
#2972=CIRCLE('',#8226,2.6) ;
#2973=CIRCLE('',#8228,1.5) ;
#2974=CIRCLE('',#8230,1.5) ;
#2975=CIRCLE('',#8232,1.2) ;
#3623=VERTEX_POINT('',#12868) ;
#3624=VERTEX_POINT('',#12870) ;
#3625=VERTEX_POINT('',#12874) ;
#3626=VERTEX_POINT('',#12878) ;
#3627=VERTEX_POINT('',#12882) ;
#3628=VERTEX_POINT('',#12887) ;
#3629=VERTEX_POINT('',#12888) ;
#3630=VERTEX_POINT('',#12890) ;
#3631=VERTEX_POINT('',#12892) ;
#3632=VERTEX_POINT('',#12896) ;
#3633=VERTEX_POINT('',#12897) ;
#3634=VERTEX_POINT('',#12899) ;
#3635=VERTEX_POINT('',#12901) ;
#3636=VERTEX_POINT('',#12905) ;
#3637=VERTEX_POINT('',#12907) ;
#3638=VERTEX_POINT('',#12911) ;
#3639=VERTEX_POINT('',#12912) ;
#3640=VERTEX_POINT('',#12917) ;
#3641=VERTEX_POINT('',#12921) ;
#3642=VERTEX_POINT('',#12925) ;
#3643=VERTEX_POINT('',#12929) ;
#3644=VERTEX_POINT('',#12933) ;
#3645=VERTEX_POINT('',#12935) ;
#3646=VERTEX_POINT('',#12938) ;
#3647=VERTEX_POINT('',#12940) ;
#3648=VERTEX_POINT('',#12944) ;
#3649=VERTEX_POINT('',#12945) ;
#3650=VERTEX_POINT('',#12957) ;
#3651=VERTEX_POINT('',#12959) ;
#4558=EDGE_CURVE('',#3623,#3623,#2971,.T.) ;
#4559=EDGE_CURVE('',#3623,#3624,#2051,.T.) ;
#4560=EDGE_CURVE('',#3624,#3624,#2972,.T.) ;
#4561=EDGE_CURVE('',#3624,#3625,#2052,.T.) ;
#4562=EDGE_CURVE('',#3625,#3625,#2973,.T.) ;
#4563=EDGE_CURVE('',#3625,#3626,#2053,.T.) ;
#4564=EDGE_CURVE('',#3626,#3626,#2974,.T.) ;
#4565=EDGE_CURVE('',#3626,#3627,#2054,.T.) ;
#4566=EDGE_CURVE('',#3627,#3627,#2975,.T.) ;
#4567=EDGE_CURVE('',#3628,#3629,#2055,.T.) ;
#4568=EDGE_CURVE('',#3628,#3630,#2056,.T.) ;
#4569=EDGE_CURVE('',#3630,#3631,#2057,.T.) ;
#4570=EDGE_CURVE('',#3629,#3631,#2058,.T.) ;
#4571=EDGE_CURVE('',#3632,#3633,#2059,.T.) ;
#4572=EDGE_CURVE('',#3632,#3634,#2060,.F.) ;
#4573=EDGE_CURVE('',#3634,#3635,#2061,.T.) ;
#4574=EDGE_CURVE('',#3633,#3635,#2062,.F.) ;
#4575=EDGE_CURVE('',#3630,#3636,#2063,.T.) ;
#4576=EDGE_CURVE('',#3636,#3637,#2064,.T.) ;
#4577=EDGE_CURVE('',#3631,#3637,#2065,.T.) ;
#4578=EDGE_CURVE('',#3638,#3639,#2066,.T.) ;
#4579=EDGE_CURVE('',#3638,#3632,#2067,.F.) ;
#4580=EDGE_CURVE('',#3639,#3633,#2068,.F.) ;
#4581=EDGE_CURVE('',#3637,#3640,#2069,.T.) ;
#4582=EDGE_CURVE('',#3640,#3629,#2070,.T.) ;
#4583=EDGE_CURVE('',#3641,#3639,#2071,.F.) ;
#4584=EDGE_CURVE('',#3641,#3635,#2072,.T.) ;
#4585=EDGE_CURVE('',#3642,#3628,#2073,.T.) ;
#4586=EDGE_CURVE('',#3636,#3642,#2074,.T.) ;
#4587=EDGE_CURVE('',#3643,#3634,#2075,.T.) ;
#4588=EDGE_CURVE('',#3643,#3638,#2076,.F.) ;
#4589=EDGE_CURVE('',#3642,#3644,#2077,.F.) ;
#4590=EDGE_CURVE('',#3644,#3645,#2078,.T.) ;
#4591=EDGE_CURVE('',#3643,#3645,#2079,.F.) ;
#4592=EDGE_CURVE('',#3646,#3641,#2080,.T.) ;
#4593=EDGE_CURVE('',#3647,#3646,#2081,.T.) ;
#4594=EDGE_CURVE('',#3647,#3640,#2082,.T.) ;
#4595=EDGE_CURVE('',#3648,#3649,#2083,.T.) ;
#4596=EDGE_CURVE('',#3648,#3628,#2084,.F.) ;
#4597=EDGE_CURVE('',#3628,#3634,#2085,.T.) ;
#4598=EDGE_CURVE('',#3649,#3634,#2086,.F.) ;
#4599=EDGE_CURVE('',#3644,#3648,#2087,.F.) ;
#4600=EDGE_CURVE('',#3645,#3649,#2088,.F.) ;
#4601=EDGE_CURVE('',#3629,#3635,#2089,.T.) ;
#4602=EDGE_CURVE('',#3629,#3650,#2090,.T.) ;
#4603=EDGE_CURVE('',#3650,#3651,#2091,.T.) ;
#4604=EDGE_CURVE('',#3635,#3651,#2092,.T.) ;
#4605=EDGE_CURVE('',#3650,#3647,#2093,.T.) ;
#4606=EDGE_CURVE('',#3651,#3646,#2094,.T.) ;
#6342=ORIENTED_EDGE('',*,*,#4558,.F.) ;
#6343=ORIENTED_EDGE('',*,*,#4559,.T.) ;
#6344=ORIENTED_EDGE('',*,*,#4560,.T.) ;
#6345=ORIENTED_EDGE('',*,*,#4559,.F.) ;
#6346=ORIENTED_EDGE('',*,*,#4560,.F.) ;
#6347=ORIENTED_EDGE('',*,*,#4561,.T.) ;
#6348=ORIENTED_EDGE('',*,*,#4562,.T.) ;
#6349=ORIENTED_EDGE('',*,*,#4561,.F.) ;
#6350=ORIENTED_EDGE('',*,*,#4562,.F.) ;
#6351=ORIENTED_EDGE('',*,*,#4563,.T.) ;
#6352=ORIENTED_EDGE('',*,*,#4564,.T.) ;
#6353=ORIENTED_EDGE('',*,*,#4563,.F.) ;
#6354=ORIENTED_EDGE('',*,*,#4564,.F.) ;
#6355=ORIENTED_EDGE('',*,*,#4565,.T.) ;
#6356=ORIENTED_EDGE('',*,*,#4566,.T.) ;
#6357=ORIENTED_EDGE('',*,*,#4565,.F.) ;
#6358=ORIENTED_EDGE('',*,*,#4566,.F.) ;
#6359=ORIENTED_EDGE('',*,*,#4567,.F.) ;
#6360=ORIENTED_EDGE('',*,*,#4568,.T.) ;
#6361=ORIENTED_EDGE('',*,*,#4569,.T.) ;
#6362=ORIENTED_EDGE('',*,*,#4570,.F.) ;
#6363=ORIENTED_EDGE('',*,*,#4571,.F.) ;
#6364=ORIENTED_EDGE('',*,*,#4572,.T.) ;
#6365=ORIENTED_EDGE('',*,*,#4573,.T.) ;
#6366=ORIENTED_EDGE('',*,*,#4574,.F.) ;
#6367=ORIENTED_EDGE('',*,*,#4569,.F.) ;
#6368=ORIENTED_EDGE('',*,*,#4575,.T.) ;
#6369=ORIENTED_EDGE('',*,*,#4576,.T.) ;
#6370=ORIENTED_EDGE('',*,*,#4577,.F.) ;
#6371=ORIENTED_EDGE('',*,*,#4578,.F.) ;
#6372=ORIENTED_EDGE('',*,*,#4579,.T.) ;
#6373=ORIENTED_EDGE('',*,*,#4571,.T.) ;
#6374=ORIENTED_EDGE('',*,*,#4580,.F.) ;
#6375=ORIENTED_EDGE('',*,*,#4570,.T.) ;
#6376=ORIENTED_EDGE('',*,*,#4577,.T.) ;
#6377=ORIENTED_EDGE('',*,*,#4581,.T.) ;
#6378=ORIENTED_EDGE('',*,*,#4582,.T.) ;
#6379=ORIENTED_EDGE('',*,*,#4583,.T.) ;
#6380=ORIENTED_EDGE('',*,*,#4580,.T.) ;
#6381=ORIENTED_EDGE('',*,*,#4574,.T.) ;
#6382=ORIENTED_EDGE('',*,*,#4584,.F.) ;
#6383=ORIENTED_EDGE('',*,*,#4585,.F.) ;
#6384=ORIENTED_EDGE('',*,*,#4586,.F.) ;
#6385=ORIENTED_EDGE('',*,*,#4575,.F.) ;
#6386=ORIENTED_EDGE('',*,*,#4568,.F.) ;
#6387=ORIENTED_EDGE('',*,*,#4587,.T.) ;
#6388=ORIENTED_EDGE('',*,*,#4572,.F.) ;
#6389=ORIENTED_EDGE('',*,*,#4579,.F.) ;
#6390=ORIENTED_EDGE('',*,*,#4588,.F.) ;
#6391=ORIENTED_EDGE('',*,*,#4558,.T.) ;
#6392=ORIENTED_EDGE('',*,*,#4581,.F.) ;
#6393=ORIENTED_EDGE('',*,*,#4576,.F.) ;
#6394=ORIENTED_EDGE('',*,*,#4586,.T.) ;
#6395=ORIENTED_EDGE('',*,*,#4589,.T.) ;
#6396=ORIENTED_EDGE('',*,*,#4590,.T.) ;
#6397=ORIENTED_EDGE('',*,*,#4591,.F.) ;
#6398=ORIENTED_EDGE('',*,*,#4588,.T.) ;
#6399=ORIENTED_EDGE('',*,*,#4578,.T.) ;
#6400=ORIENTED_EDGE('',*,*,#4583,.F.) ;
#6401=ORIENTED_EDGE('',*,*,#4592,.F.) ;
#6402=ORIENTED_EDGE('',*,*,#4593,.F.) ;
#6403=ORIENTED_EDGE('',*,*,#4594,.T.) ;
#6404=ORIENTED_EDGE('',*,*,#4595,.F.) ;
#6405=ORIENTED_EDGE('',*,*,#4596,.T.) ;
#6406=ORIENTED_EDGE('',*,*,#4597,.T.) ;
#6407=ORIENTED_EDGE('',*,*,#4598,.F.) ;
#6408=ORIENTED_EDGE('',*,*,#4590,.F.) ;
#6409=ORIENTED_EDGE('',*,*,#4599,.T.) ;
#6410=ORIENTED_EDGE('',*,*,#4595,.T.) ;
#6411=ORIENTED_EDGE('',*,*,#4600,.F.) ;
#6412=ORIENTED_EDGE('',*,*,#4585,.T.) ;
#6413=ORIENTED_EDGE('',*,*,#4596,.F.) ;
#6414=ORIENTED_EDGE('',*,*,#4599,.F.) ;
#6415=ORIENTED_EDGE('',*,*,#4589,.F.) ;
#6416=ORIENTED_EDGE('',*,*,#4591,.T.) ;
#6417=ORIENTED_EDGE('',*,*,#4600,.T.) ;
#6418=ORIENTED_EDGE('',*,*,#4598,.T.) ;
#6419=ORIENTED_EDGE('',*,*,#4587,.F.) ;
#6420=ORIENTED_EDGE('',*,*,#4601,.F.) ;
#6421=ORIENTED_EDGE('',*,*,#4602,.T.) ;
#6422=ORIENTED_EDGE('',*,*,#4603,.T.) ;
#6423=ORIENTED_EDGE('',*,*,#4604,.F.) ;
#6424=ORIENTED_EDGE('',*,*,#4582,.F.) ;
#6425=ORIENTED_EDGE('',*,*,#4594,.F.) ;
#6426=ORIENTED_EDGE('',*,*,#4605,.F.) ;
#6427=ORIENTED_EDGE('',*,*,#4602,.F.) ;
#6428=ORIENTED_EDGE('',*,*,#4603,.F.) ;
#6429=ORIENTED_EDGE('',*,*,#4605,.T.) ;
#6430=ORIENTED_EDGE('',*,*,#4593,.T.) ;
#6431=ORIENTED_EDGE('',*,*,#4606,.F.) ;
#6432=ORIENTED_EDGE('',*,*,#4604,.T.) ;
#6433=ORIENTED_EDGE('',*,*,#4606,.T.) ;
#6434=ORIENTED_EDGE('',*,*,#4592,.T.) ;
#6435=ORIENTED_EDGE('',*,*,#4584,.T.) ;
#6436=ORIENTED_EDGE('',*,*,#4597,.F.) ;
#6437=ORIENTED_EDGE('',*,*,#4567,.T.) ;
#6438=ORIENTED_EDGE('',*,*,#4601,.T.) ;
#6439=ORIENTED_EDGE('',*,*,#4573,.F.) ;
#6892=CONICAL_SURFACE('',#8227,1.5,0.785398163397) ;
#6893=CONICAL_SURFACE('',#8231,1.2,0.785398163397) ;
#7222=ADVANCED_FACE('',(#972),#642,.T.) ;
#7223=ADVANCED_FACE('',(#973),#6892,.T.) ;
#7224=ADVANCED_FACE('',(#974),#643,.T.) ;
#7225=ADVANCED_FACE('',(#975),#6893,.T.) ;
#7226=ADVANCED_FACE('',(#976),#435,.F.) ;
#7227=ADVANCED_FACE('',(#977),#436,.T.) ;
#7228=ADVANCED_FACE('',(#978),#437,.F.) ;
#7229=ADVANCED_FACE('',(#979),#438,.T.) ;
#7230=ADVANCED_FACE('',(#980),#439,.F.) ;
#7231=ADVANCED_FACE('',(#981),#440,.T.) ;
#7232=ADVANCED_FACE('',(#982),#441,.T.) ;
#7233=ADVANCED_FACE('',(#983),#442,.F.) ;
#7234=ADVANCED_FACE('',(#984),#443,.F.) ;
#7235=ADVANCED_FACE('',(#985,#245),#444,.T.) ;
#7236=ADVANCED_FACE('',(#986),#445,.F.) ;
#7237=ADVANCED_FACE('',(#987),#446,.F.) ;
#7238=ADVANCED_FACE('',(#988),#447,.F.) ;
#7239=ADVANCED_FACE('',(#989),#448,.T.) ;
#7240=ADVANCED_FACE('',(#990),#449,.T.) ;
#7241=ADVANCED_FACE('',(#991),#450,.F.) ;
#7242=ADVANCED_FACE('',(#992),#451,.T.) ;
#7243=ADVANCED_FACE('',(#993),#452,.T.) ;
#7244=ADVANCED_FACE('',(#994),#453,.T.) ;
#7380=CLOSED_SHELL('',(#7222,#7223,#7224,#7225,#7226,#7227,#7228,#7229,
#7230,#7231,#7232,#7233,#7234,#7235,#7236,#7237,#7238,#7239,#7240,#7241,
#7242,#7243,#7244)) ;
#8223=AXIS2_PLACEMENT_3D('',#12866,#10275,#10276) ;
#8224=AXIS2_PLACEMENT_3D('',#12867,#10277,#10278) ;
#8225=AXIS2_PLACEMENT_3D('',#12869,#10279,#10280) ;
#8226=AXIS2_PLACEMENT_3D('',#12872,#10282,#10283) ;
#8227=AXIS2_PLACEMENT_3D('',#12873,#10284,#10285) ;
#8228=AXIS2_PLACEMENT_3D('',#12876,#10287,#10288) ;
#8229=AXIS2_PLACEMENT_3D('',#12877,#10289,#10290) ;
#8230=AXIS2_PLACEMENT_3D('',#12880,#10292,#10293) ;
#8231=AXIS2_PLACEMENT_3D('',#12881,#10294,#10295) ;
#8232=AXIS2_PLACEMENT_3D('',#12884,#10297,#10298) ;
#8233=AXIS2_PLACEMENT_3D('',#12885,#10299,#10300) ;
#8234=AXIS2_PLACEMENT_3D('',#12886,#10301,#10302) ;
#8235=AXIS2_PLACEMENT_3D('',#12895,#10307,#10308) ;
#8236=AXIS2_PLACEMENT_3D('',#12904,#10313,#10314) ;
#8237=AXIS2_PLACEMENT_3D('',#12910,#10318,#10319) ;
#8238=AXIS2_PLACEMENT_3D('',#12916,#10323,#10324) ;
#8239=AXIS2_PLACEMENT_3D('',#12920,#10327,#10328) ;
#8240=AXIS2_PLACEMENT_3D('',#12924,#10331,#10332) ;
#8241=AXIS2_PLACEMENT_3D('',#12928,#10335,#10336) ;
#8242=AXIS2_PLACEMENT_3D('',#12932,#10339,#10340) ;
#8243=AXIS2_PLACEMENT_3D('',#12943,#10347,#10348) ;
#8244=AXIS2_PLACEMENT_3D('',#12950,#10353,#10354) ;
#8245=AXIS2_PLACEMENT_3D('',#12953,#10357,#10358) ;
#8246=AXIS2_PLACEMENT_3D('',#12954,#10359,#10360) ;
#8247=AXIS2_PLACEMENT_3D('',#12955,#10361,#10362) ;
#8248=AXIS2_PLACEMENT_3D('',#12962,#10367,#10368) ;
#8249=AXIS2_PLACEMENT_3D('',#12964,#10370,#10371) ;
#8250=AXIS2_PLACEMENT_3D('',#12966,#10373,#10374) ;
#8251=AXIS2_PLACEMENT_3D('',#12967,#10375,#10376) ;
#10275=DIRECTION('axis',(0.,0.,1.)) ;
#10276=DIRECTION('refdir',(1.,0.,0.)) ;
#10277=DIRECTION('center_axis',(0.,0.,1.)) ;
#10278=DIRECTION('ref_axis',(0.520296023213257,0.853985976599423,0.)) ;
#10279=DIRECTION('center_axis',(0.,0.,1.)) ;
#10280=DIRECTION('ref_axis',(-1.,0.,0.)) ;
#10281=DIRECTION('',(0.,0.,-1.)) ;
#10282=DIRECTION('center_axis',(0.,0.,1.)) ;
#10283=DIRECTION('ref_axis',(-1.,0.,0.)) ;
#10284=DIRECTION('center_axis',(0.,0.,1.)) ;
#10285=DIRECTION('ref_axis',(0.520296023213257,0.853985976599423,0.)) ;
#10286=DIRECTION('',(0.367904846238322,0.603859275091397,-0.707106781186864)) ;
#10287=DIRECTION('center_axis',(0.,0.,1.)) ;
#10288=DIRECTION('ref_axis',(-1.,0.,0.)) ;
#10289=DIRECTION('center_axis',(0.,0.,1.)) ;
#10290=DIRECTION('ref_axis',(0.520296023213257,0.853985976599423,0.)) ;
#10291=DIRECTION('',(0.,0.,-1.)) ;
#10292=DIRECTION('center_axis',(0.,0.,1.)) ;
#10293=DIRECTION('ref_axis',(-1.,0.,0.)) ;
#10294=DIRECTION('center_axis',(0.,0.,1.)) ;
#10295=DIRECTION('ref_axis',(0.520296023213257,0.853985976599423,0.)) ;
#10296=DIRECTION('',(0.367904846238322,0.603859275091397,-0.707106781186864)) ;
#10297=DIRECTION('center_axis',(0.,0.,1.)) ;
#10298=DIRECTION('ref_axis',(-1.,0.,0.)) ;
#10299=DIRECTION('center_axis',(0.,0.,1.)) ;
#10300=DIRECTION('ref_axis',(1.,0.,0.)) ;
#10301=DIRECTION('center_axis',(0.612372435695786,0.353553390592877,0.707106781186753)) ;
#10302=DIRECTION('ref_axis',(-0.612372435696143,-0.353553390593082,0.707106781186342)) ;
#10303=DIRECTION('',(0.50000000000019,-0.866025403784329,0.)) ;
#10304=DIRECTION('',(-0.612372435695786,-0.353553390592877,0.707106781186753)) ;
#10305=DIRECTION('',(0.50000000000019,-0.866025403784329,0.)) ;
#10306=DIRECTION('',(-0.612372435695786,-0.353553390592877,0.707106781186753)) ;
#10307=DIRECTION('center_axis',(0.612372435695786,0.353553390592877,-0.707106781186753)) ;
#10308=DIRECTION('ref_axis',(0.612372435696143,0.353553390593082,0.707106781186342)) ;
#10309=DIRECTION('',(0.50000000000019,-0.866025403784329,0.)) ;
#10310=DIRECTION('',(0.612372435695786,0.353553390592877,0.707106781186753)) ;
#10311=DIRECTION('',(0.50000000000019,-0.866025403784329,0.)) ;
#10312=DIRECTION('',(0.612372435695786,0.353553390592877,0.707106781186753)) ;
#10313=DIRECTION('center_axis',(0.866025403784329,0.50000000000019,0.)) ;
#10314=DIRECTION('ref_axis',(0.,0.,1.)) ;
#10315=DIRECTION('',(0.,0.,1.)) ;
#10316=DIRECTION('',(0.50000000000019,-0.866025403784329,0.)) ;
#10317=DIRECTION('',(0.,0.,1.)) ;
#10318=DIRECTION('center_axis',(0.866025403784329,0.50000000000019,0.)) ;
#10319=DIRECTION('ref_axis',(0.,0.,1.)) ;
#10320=DIRECTION('',(0.50000000000019,-0.866025403784329,0.)) ;
#10321=DIRECTION('',(0.,0.,1.)) ;
#10322=DIRECTION('',(0.,0.,1.)) ;
#10323=DIRECTION('center_axis',(-0.50000000000019,0.866025403784329,0.)) ;
#10324=DIRECTION('ref_axis',(-0.866025403784329,-0.50000000000019,0.)) ;
#10325=DIRECTION('',(0.866025403784329,0.50000000000019,0.)) ;
#10326=DIRECTION('',(0.,0.,-1.)) ;
#10327=DIRECTION('center_axis',(-0.50000000000019,0.866025403784329,0.)) ;
#10328=DIRECTION('ref_axis',(-0.866025403784329,-0.50000000000019,0.)) ;
#10329=DIRECTION('',(-0.866025403784329,-0.50000000000019,0.)) ;
#10330=DIRECTION('',(0.,0.,-1.)) ;
#10331=DIRECTION('center_axis',(-0.50000000000019,0.866025403784329,0.)) ;
#10332=DIRECTION('ref_axis',(-0.866025403784329,-0.50000000000019,0.)) ;
#10333=DIRECTION('',(0.,0.,-1.)) ;
#10334=DIRECTION('',(0.866025403784329,0.50000000000019,0.)) ;
#10335=DIRECTION('center_axis',(-0.50000000000019,0.866025403784329,0.)) ;
#10336=DIRECTION('ref_axis',(-0.866025403784329,-0.50000000000019,0.)) ;
#10337=DIRECTION('',(0.,0.,-1.)) ;
#10338=DIRECTION('',(-0.866025403784329,-0.50000000000019,0.)) ;
#10339=DIRECTION('center_axis',(0.,0.,1.)) ;
#10340=DIRECTION('ref_axis',(1.,0.,0.)) ;
#10341=DIRECTION('',(0.50000000000019,-0.866025403784329,0.)) ;
#10342=DIRECTION('',(0.866025403784329,0.50000000000019,0.)) ;
#10343=DIRECTION('',(0.50000000000019,-0.866025403784329,0.)) ;
#10344=DIRECTION('',(-0.50000000000019,0.866025403784329,0.)) ;
#10345=DIRECTION('',(0.866025403784329,0.50000000000019,0.)) ;
#10346=DIRECTION('',(-0.50000000000019,0.866025403784329,0.)) ;
#10347=DIRECTION('center_axis',(-0.353553390592877,0.612372435695786,-0.707106781186753)) ;
#10348=DIRECTION('ref_axis',(-0.353553390593082,0.612372435696143,0.707106781186342)) ;
#10349=DIRECTION('',(0.866025403784329,0.50000000000019,0.)) ;
#10350=DIRECTION('',(-0.353553390592877,0.612372435695786,0.707106781186753)) ;
#10351=DIRECTION('',(0.866025403784329,0.50000000000019,0.)) ;
#10352=DIRECTION('',(-0.353553390592877,0.612372435695786,0.707106781186753)) ;
#10353=DIRECTION('center_axis',(-0.50000000000019,0.866025403784329,0.)) ;
#10354=DIRECTION('ref_axis',(0.,0.,1.)) ;
#10355=DIRECTION('',(0.,0.,1.)) ;
#10356=DIRECTION('',(0.,0.,1.)) ;
#10357=DIRECTION('center_axis',(-0.866025403784329,-0.50000000000019,0.)) ;
#10358=DIRECTION('ref_axis',(0.50000000000019,-0.866025403784329,0.)) ;
#10359=DIRECTION('center_axis',(-0.866025403784329,-0.50000000000019,0.)) ;
#10360=DIRECTION('ref_axis',(0.50000000000019,-0.866025403784329,0.)) ;
#10361=DIRECTION('center_axis',(-0.353553390592877,0.612372435695786,0.707106781186753)) ;
#10362=DIRECTION('ref_axis',(0.353553390593082,-0.612372435696143,0.707106781186342)) ;
#10363=DIRECTION('',(0.866025403784329,0.50000000000019,0.)) ;
#10364=DIRECTION('',(0.353553390592877,-0.612372435695786,0.707106781186753)) ;
#10365=DIRECTION('',(0.866025403784329,0.50000000000019,0.)) ;
#10366=DIRECTION('',(0.353553390592877,-0.612372435695786,0.707106781186753)) ;
#10367=DIRECTION('center_axis',(-0.866025403784329,-0.50000000000019,0.)) ;
#10368=DIRECTION('ref_axis',(0.50000000000019,-0.866025403784329,0.)) ;
#10369=DIRECTION('',(0.,0.,1.)) ;
#10370=DIRECTION('center_axis',(-0.50000000000019,0.866025403784329,0.)) ;
#10371=DIRECTION('ref_axis',(0.,0.,1.)) ;
#10372=DIRECTION('',(0.,0.,1.)) ;
#10373=DIRECTION('center_axis',(-0.866025403784329,-0.50000000000019,0.)) ;
#10374=DIRECTION('ref_axis',(0.50000000000019,-0.866025403784329,0.)) ;
#10375=DIRECTION('center_axis',(0.,0.,1.)) ;
#10376=DIRECTION('ref_axis',(0.,1.,0.)) ;
#12866=CARTESIAN_POINT('',(0.,0.,0.)) ;
#12867=CARTESIAN_POINT('Origin',(21.6506350946,12.5,128.75)) ;
#12868=CARTESIAN_POINT('',(20.2978654343,10.2796364608,143.75)) ;
#12869=CARTESIAN_POINT('Origin',(21.6506350946,12.5,143.75)) ;
#12870=CARTESIAN_POINT('',(20.2978654343,10.2796364608,143.25)) ;
#12871=CARTESIAN_POINT('',(20.2978654342455,10.2796364608415,128.75)) ;
#12872=CARTESIAN_POINT('Origin',(21.6506350946,12.5,143.25)) ;
#12873=CARTESIAN_POINT('Origin',(21.6506350946,12.5,142.15)) ;
#12874=CARTESIAN_POINT('',(20.8701910598,11.2190210351,142.15)) ;
#12875=CARTESIAN_POINT('',(20.8701910597801,11.2190210351009,142.15)) ;
#12876=CARTESIAN_POINT('Origin',(21.6506350946,12.5,142.15)) ;
#12877=CARTESIAN_POINT('Origin',(21.6506350946,12.5,128.75)) ;
#12878=CARTESIAN_POINT('',(20.8701910598,11.2190210351,114.05)) ;
#12879=CARTESIAN_POINT('',(20.8701910597801,11.2190210351009,128.75)) ;
#12880=CARTESIAN_POINT('Origin',(21.6506350946,12.5,114.05)) ;
#12881=CARTESIAN_POINT('Origin',(21.6506350946,12.5,113.75)) ;
#12882=CARTESIAN_POINT('',(21.0262798668,11.4752168281,113.75)) ;
#12883=CARTESIAN_POINT('',(21.0262798667441,11.4752168280807,113.75)) ;
#12884=CARTESIAN_POINT('Origin',(21.6506350946,12.5,113.75)) ;
#12885=CARTESIAN_POINT('Origin',(0.,-26.2,113.75)) ;
#12886=CARTESIAN_POINT('Origin',(21.3042249331,12.3,142.25)) ;
#12887=CARTESIAN_POINT('',(21.1042249331,12.6464101615,142.25)) ;
#12888=CARTESIAN_POINT('',(21.5042249331,11.9535898385,142.25)) ;
#12889=CARTESIAN_POINT('',(21.4042249331,12.1267949192,142.25)) ;
#12890=CARTESIAN_POINT('',(19.935090638,11.9714101615,143.6)) ;
#12891=CARTESIAN_POINT('',(20.5196577855,12.3089101615,142.925)) ;
#12892=CARTESIAN_POINT('',(20.335090638,11.2785898385,143.6)) ;
#12893=CARTESIAN_POINT('',(20.135090638,11.625,143.6)) ;
#12894=CARTESIAN_POINT('',(20.9196577855,11.6160898385,142.925)) ;
#12895=CARTESIAN_POINT('Origin',(21.9970452561,12.7,142.25)) ;
#12896=CARTESIAN_POINT('',(22.9661795512,13.7214101615,143.6)) ;
#12897=CARTESIAN_POINT('',(23.3661795512,13.0285898385,143.6)) ;
#12898=CARTESIAN_POINT('',(23.1661795512,13.375,143.6)) ;
#12899=CARTESIAN_POINT('',(21.7970452561,13.0464101615,142.25)) ;
#12900=CARTESIAN_POINT('',(22.3816124037,13.3839101615,142.925)) ;
#12901=CARTESIAN_POINT('',(22.1970452561,12.3535898385,142.25)) ;
#12902=CARTESIAN_POINT('',(21.8970452561,12.8732050808,142.25)) ;
#12903=CARTESIAN_POINT('',(22.7816124037,12.6910898385,142.925)) ;
#12904=CARTESIAN_POINT('Origin',(20.135090638,11.625,143.6)) ;
#12905=CARTESIAN_POINT('',(19.935090638,11.9714101615,143.75)) ;
#12906=CARTESIAN_POINT('',(19.935090638,11.9714101615,143.675)) ;
#12907=CARTESIAN_POINT('',(20.335090638,11.2785898385,143.75)) ;
#12908=CARTESIAN_POINT('',(20.135090638,11.625,143.75)) ;
#12909=CARTESIAN_POINT('',(20.335090638,11.2785898385,143.675)) ;
#12910=CARTESIAN_POINT('Origin',(23.1661795512,13.375,143.6)) ;
#12911=CARTESIAN_POINT('',(22.9661795512,13.7214101615,143.75)) ;
#12912=CARTESIAN_POINT('',(23.3661795512,13.0285898385,143.75)) ;
#12913=CARTESIAN_POINT('',(23.1661795512,13.375,143.75)) ;
#12914=CARTESIAN_POINT('',(22.9661795512,13.7214101615,143.675)) ;
#12915=CARTESIAN_POINT('',(23.3661795512,13.0285898385,143.675)) ;
#12916=CARTESIAN_POINT('Origin',(0.2,-0.346410161514,0.)) ;
#12917=CARTESIAN_POINT('',(21.5042249331,11.9535898385,143.75)) ;
#12918=CARTESIAN_POINT('',(20.9196577855,11.6160898385,143.75)) ;
#12919=CARTESIAN_POINT('',(21.5042249331,11.9535898385,143.)) ;
#12920=CARTESIAN_POINT('Origin',(0.2,-0.346410161514,0.)) ;
#12921=CARTESIAN_POINT('',(22.1970452561,12.3535898385,143.75)) ;
#12922=CARTESIAN_POINT('',(22.7816124037,12.6910898385,143.75)) ;
#12923=CARTESIAN_POINT('',(22.1970452561,12.3535898385,143.)) ;
#12924=CARTESIAN_POINT('Origin',(-0.2,0.346410161514,0.)) ;
#12925=CARTESIAN_POINT('',(21.1042249331,12.6464101615,143.75)) ;
#12926=CARTESIAN_POINT('',(21.1042249331,12.6464101615,143.)) ;
#12927=CARTESIAN_POINT('',(20.5196577855,12.3089101615,143.75)) ;
#12928=CARTESIAN_POINT('Origin',(-0.2,0.346410161514,0.)) ;
#12929=CARTESIAN_POINT('',(21.7970452561,13.0464101615,143.75)) ;
#12930=CARTESIAN_POINT('',(21.7970452561,13.0464101615,143.)) ;
#12931=CARTESIAN_POINT('',(22.3816124037,13.3839101615,143.75)) ;
#12932=CARTESIAN_POINT('Origin',(0.,-25.,143.75)) ;
#12933=CARTESIAN_POINT('',(20.4292249331,13.8155444566,143.75)) ;
#12934=CARTESIAN_POINT('',(20.7667249331,13.2309773091,143.75)) ;
#12935=CARTESIAN_POINT('',(21.1220452561,14.2155444566,143.75)) ;
#12936=CARTESIAN_POINT('',(20.7756350946,14.0155444566,143.75)) ;
#12937=CARTESIAN_POINT('',(21.4595452561,13.6309773091,143.75)) ;
#12938=CARTESIAN_POINT('',(22.8720452561,11.1844555434,143.75)) ;
#12939=CARTESIAN_POINT('',(22.5345452561,11.7690226909,143.75)) ;
#12940=CARTESIAN_POINT('',(22.1792249331,10.7844555434,143.75)) ;
#12941=CARTESIAN_POINT('',(22.5256350946,10.9844555434,143.75)) ;
#12942=CARTESIAN_POINT('',(21.8417249331,11.3690226909,143.75)) ;
#12943=CARTESIAN_POINT('Origin',(21.4506350946,12.8464101615,142.25)) ;
#12944=CARTESIAN_POINT('',(20.4292249331,13.8155444566,143.6)) ;
#12945=CARTESIAN_POINT('',(21.1220452561,14.2155444566,143.6)) ;
#12946=CARTESIAN_POINT('',(20.7756350946,14.0155444566,143.6)) ;
#12947=CARTESIAN_POINT('',(20.7667249331,13.2309773091,142.925)) ;
#12948=CARTESIAN_POINT('',(21.2774300139,12.7464101615,142.25)) ;
#12949=CARTESIAN_POINT('',(21.4595452561,13.6309773091,142.925)) ;
#12950=CARTESIAN_POINT('Origin',(20.7756350946,14.0155444566,143.6)) ;
#12951=CARTESIAN_POINT('',(20.4292249331,13.8155444566,143.675)) ;
#12952=CARTESIAN_POINT('',(21.1220452561,14.2155444566,143.675)) ;
#12953=CARTESIAN_POINT('Origin',(33.8042249331,-9.35063509461,0.)) ;
#12954=CARTESIAN_POINT('Origin',(34.4970452561,-8.95063509461,0.)) ;
#12955=CARTESIAN_POINT('Origin',(21.8506350946,12.1535898385,142.25)) ;
#12956=CARTESIAN_POINT('',(22.0238401754,12.2535898385,142.25)) ;
#12957=CARTESIAN_POINT('',(22.1792249331,10.7844555434,143.6)) ;
#12958=CARTESIAN_POINT('',(21.8417249331,11.3690226909,142.925)) ;
#12959=CARTESIAN_POINT('',(22.8720452561,11.1844555434,143.6)) ;
#12960=CARTESIAN_POINT('',(22.5256350946,10.9844555434,143.6)) ;
#12961=CARTESIAN_POINT('',(22.5345452561,11.7690226909,142.925)) ;
#12962=CARTESIAN_POINT('Origin',(33.8042249331,-9.35063509461,0.)) ;
#12963=CARTESIAN_POINT('',(22.1792249331,10.7844555434,143.675)) ;
#12964=CARTESIAN_POINT('Origin',(22.5256350946,10.9844555434,143.6)) ;
#12965=CARTESIAN_POINT('',(22.8720452561,11.1844555434,143.675)) ;
#12966=CARTESIAN_POINT('Origin',(34.4970452561,-8.95063509461,0.)) ;
#12967=CARTESIAN_POINT('Origin',(0.,-25.,142.25)) ;
#13486=UNCERTAINTY_MEASURE_WITH_UNIT(LENGTH_MEASURE(0.01),#13511,
'DISTANCE_ACCURACY_VALUE',
'Maximum model space distance between geometric entities at asserted c
onnectivities') ;
#13493=UNCERTAINTY_MEASURE_WITH_UNIT(LENGTH_MEASURE(0.01),#13511,
'DISTANCE_ACCURACY_VALUE',
'Maximum model space distance between geometric entities at asserted c
onnectivities') ;
#13503=(
GEOMETRIC_REPRESENTATION_CONTEXT(3)
GLOBAL_UNCERTAINTY_ASSIGNED_CONTEXT((#13486))
GLOBAL_UNIT_ASSIGNED_CONTEXT((#13511,#13513,#13514))
REPRESENTATION_CONTEXT('','3D')
) ;
#13510=(
GEOMETRIC_REPRESENTATION_CONTEXT(3)
GLOBAL_UNCERTAINTY_ASSIGNED_CONTEXT((#13493))
GLOBAL_UNIT_ASSIGNED_CONTEXT((#13511,#13513,#13514))
REPRESENTATION_CONTEXT('','3D')
) ;
#13511=(
LENGTH_UNIT()
NAMED_UNIT(*)
SI_UNIT(.MILLI.,.METRE.)
) ;
#13513=(
NAMED_UNIT(*)
PLANE_ANGLE_UNIT()
SI_UNIT($,.RADIAN.)
) ;
#13514=(
NAMED_UNIT(*)
SI_UNIT($,.STERADIAN.)
SOLID_ANGLE_UNIT()
) ;
#13524=SHAPE_DEFINITION_REPRESENTATION(#13540,#13571) ;
#13540=PRODUCT_DEFINITION_SHAPE('',$,#13588) ;
#13571=SHAPE_REPRESENTATION('',(#8223),#13503) ;
#13578=PRODUCT_DEFINITION_CONTEXT('part definition',#13628,'design') ;
#13588=PRODUCT_DEFINITION('Cover_Screw_3','Cover_Screw_3',#13604,#13578) ;
#13604=PRODUCT_DEFINITION_FORMATION('',$,#13639) ;
#13628=APPLICATION_CONTEXT(
'Core Data for Automotive Mechanical Design Process') ;
#13629=PRODUCT_CONTEXT('part definition',#13628,'mechanical') ;
#13639=PRODUCT('Cover_Screw_3','Cover_Screw_3',$,(#13629)) ;
#13650=PRESENTATION_STYLE_ASSIGNMENT((#13655)) ;
#13655=SURFACE_STYLE_USAGE(.BOTH.,#13660) ;
#13660=SURFACE_SIDE_STYLE('',(#13665)) ;
#13665=SURFACE_STYLE_FILL_AREA(#13670) ;
#13670=FILL_AREA_STYLE('Opaque(144,144,144)',(#13675)) ;
#13675=FILL_AREA_STYLE_COLOUR('Opaque(144,144,144)',#13680) ;
#13680=COLOUR_RGB('Opaque(144,144,144)', 0.40784314, 0.44705882, 0.49803922) ;
ENDSEC;
END-ISO-10303-21;
